ISO-10303-21;
HEADER;
/* Generated by software containing ST-Developer
 * from STEP Tools, Inc. (www.steptools.com) 
 */

FILE_DESCRIPTION(
/* description */ ('STEP AP214'),
/* implementation_level */ '2;1');

FILE_NAME(
/* name */ 'Hex Nut M10 x 1.5 (2).step',
/* time_stamp */ '2026-11-14T06:43:04-08:00',
/* author */ (''),
/* organization */ (''),
/* preprocessor_version */ 'ST-DEVELOPER v20.2',
/* originating_system */ 'Autodesk Translation Framework v15.17.0.0',
/* authorisation */ '');

FILE_SCHEMA (('AUTOMOTIVE_DESIGN { 1 0 10303 214 3 1 1 }'));
ENDSEC;

DATA;
#10=MECHANICAL_DESIGN_GEOMETRIC_PRESENTATION_REPRESENTATION('',(#202),#5658);
#83=CONICAL_SURFACE('',#3349,8.,1.0471975511966);
#84=CONICAL_SURFACE('',#3350,8.,1.0471975511966);
#85=CONICAL_SURFACE('',#3351,8.,1.0471975511966);
#86=CONICAL_SURFACE('',#3352,8.,1.0471975511966);
#87=CONICAL_SURFACE('',#3353,8.,1.0471975511966);
#88=CONICAL_SURFACE('',#3354,8.,1.0471975511966);
#89=CONICAL_SURFACE('',#3355,8.,1.0471975511966);
#90=CONICAL_SURFACE('',#3356,8.,1.0471975511966);
#91=CONICAL_SURFACE('',#3357,8.,1.0471975511966);
#92=CONICAL_SURFACE('',#3358,8.,1.0471975511966);
#93=CONICAL_SURFACE('',#3359,8.,1.0471975511966);
#94=CONICAL_SURFACE('',#3360,8.,1.0471975511966);
#117=(
BOUNDED_CURVE()
B_SPLINE_CURVE(2,(#4998,#4999,#5000),.UNSPECIFIED.,.F.,.F.)
B_SPLINE_CURVE_WITH_KNOTS((3,3),(1.54292191464265,2.47778215640189),
 .UNSPECIFIED.)
CURVE()
GEOMETRIC_REPRESENTATION_ITEM()
RATIONAL_B_SPLINE_CURVE((1.8727241335928,2.01757984944671,2.01757984944671))
REPRESENTATION_ITEM('')
);
#118=(
BOUNDED_CURVE()
B_SPLINE_CURVE(2,(#5002,#5003,#5004),.UNSPECIFIED.,.F.,.F.)
B_SPLINE_CURVE_WITH_KNOTS((3,3),(2.47778215640189,3.41264239816114),
 .UNSPECIFIED.)
CURVE()
GEOMETRIC_REPRESENTATION_ITEM()
RATIONAL_B_SPLINE_CURVE((2.01757984944671,2.01757984944671,1.8727241335928))
REPRESENTATION_ITEM('')
);
#119=(
BOUNDED_CURVE()
B_SPLINE_CURVE(2,(#5008,#5009,#5010),.UNSPECIFIED.,.F.,.F.)
B_SPLINE_CURVE_WITH_KNOTS((3,3),(-2.47778215640189,-1.54292191464263),
 .UNSPECIFIED.)
CURVE()
GEOMETRIC_REPRESENTATION_ITEM()
RATIONAL_B_SPLINE_CURVE((2.01757984944672,2.01757984944672,1.8727241335928))
REPRESENTATION_ITEM('')
);
#120=(
BOUNDED_CURVE()
B_SPLINE_CURVE(2,(#5011,#5012,#5013),.UNSPECIFIED.,.F.,.F.)
B_SPLINE_CURVE_WITH_KNOTS((3,3),(-3.41264239816113,-2.47778215640189),
 .UNSPECIFIED.)
CURVE()
GEOMETRIC_REPRESENTATION_ITEM()
RATIONAL_B_SPLINE_CURVE((1.8727241335928,2.01757984944671,2.01757984944671))
REPRESENTATION_ITEM('')
);
#121=(
BOUNDED_CURVE()
B_SPLINE_CURVE(2,(#5016,#5017,#5018),.UNSPECIFIED.,.F.,.F.)
B_SPLINE_CURVE_WITH_KNOTS((3,3),(1.54292191464264,2.47778215640189),
 .UNSPECIFIED.)
CURVE()
GEOMETRIC_REPRESENTATION_ITEM()
RATIONAL_B_SPLINE_CURVE((1.8727241335928,2.01757984944672,2.01757984944672))
REPRESENTATION_ITEM('')
);
#122=(
BOUNDED_CURVE()
B_SPLINE_CURVE(2,(#5020,#5021,#5022),.UNSPECIFIED.,.F.,.F.)
B_SPLINE_CURVE_WITH_KNOTS((3,3),(2.47778215640189,3.41264239816113),
 .UNSPECIFIED.)
CURVE()
GEOMETRIC_REPRESENTATION_ITEM()
RATIONAL_B_SPLINE_CURVE((2.01757984944672,2.01757984944672,1.87272413359281))
REPRESENTATION_ITEM('')
);
#123=(
BOUNDED_CURVE()
B_SPLINE_CURVE(2,(#5026,#5027,#5028),.UNSPECIFIED.,.F.,.F.)
B_SPLINE_CURVE_WITH_KNOTS((3,3),(-2.47778215640188,-1.54292191464265),
 .UNSPECIFIED.)
CURVE()
GEOMETRIC_REPRESENTATION_ITEM()
RATIONAL_B_SPLINE_CURVE((2.01757984944672,2.01757984944672,1.87272413359281))
REPRESENTATION_ITEM('')
);
#124=(
BOUNDED_CURVE()
B_SPLINE_CURVE(2,(#5029,#5030,#5031),.UNSPECIFIED.,.F.,.F.)
B_SPLINE_CURVE_WITH_KNOTS((3,3),(-3.41264239816114,-2.47778215640188),
 .UNSPECIFIED.)
CURVE()
GEOMETRIC_REPRESENTATION_ITEM()
RATIONAL_B_SPLINE_CURVE((1.8727241335928,2.01757984944672,2.01757984944672))
REPRESENTATION_ITEM('')
);
#125=(
BOUNDED_CURVE()
B_SPLINE_CURVE(2,(#5035,#5036,#5037),.UNSPECIFIED.,.F.,.F.)
B_SPLINE_CURVE_WITH_KNOTS((3,3),(1.54292191464263,2.47778215640189),
 .UNSPECIFIED.)
CURVE()
GEOMETRIC_REPRESENTATION_ITEM()
RATIONAL_B_SPLINE_CURVE((1.8727241335928,2.01757984944671,2.01757984944671))
REPRESENTATION_ITEM('')
);
#126=(
BOUNDED_CURVE()
B_SPLINE_CURVE(2,(#5041,#5042,#5043),.UNSPECIFIED.,.F.,.F.)
B_SPLINE_CURVE_WITH_KNOTS((3,3),(-3.41264239816114,-2.47778215640189),
 .UNSPECIFIED.)
CURVE()
GEOMETRIC_REPRESENTATION_ITEM()
RATIONAL_B_SPLINE_CURVE((1.8727241335928,2.01757984944671,2.01757984944671))
REPRESENTATION_ITEM('')
);
#127=(
BOUNDED_CURVE()
B_SPLINE_CURVE(2,(#5044,#5045,#5046),.UNSPECIFIED.,.F.,.F.)
B_SPLINE_CURVE_WITH_KNOTS((3,3),(-2.47778215640189,-1.54292191464264),
 .UNSPECIFIED.)
CURVE()
GEOMETRIC_REPRESENTATION_ITEM()
RATIONAL_B_SPLINE_CURVE((2.01757984944671,2.01757984944672,1.8727241335928))
REPRESENTATION_ITEM('')
);
#128=(
BOUNDED_CURVE()
B_SPLINE_CURVE(2,(#5047,#5048,#5049),.UNSPECIFIED.,.F.,.F.)
B_SPLINE_CURVE_WITH_KNOTS((3,3),(2.47778215640189,3.41264239816114),
 .UNSPECIFIED.)
CURVE()
GEOMETRIC_REPRESENTATION_ITEM()
RATIONAL_B_SPLINE_CURVE((2.01757984944671,2.01757984944672,1.8727241335928))
REPRESENTATION_ITEM('')
);
#129=(
BOUNDED_CURVE()
B_SPLINE_CURVE(2,(#5052,#5053,#5054),.UNSPECIFIED.,.F.,.F.)
B_SPLINE_CURVE_WITH_KNOTS((3,3),(1.54292191464265,2.47778215640188),
 .UNSPECIFIED.)
CURVE()
GEOMETRIC_REPRESENTATION_ITEM()
RATIONAL_B_SPLINE_CURVE((1.8727241335928,2.01757984944671,2.01757984944671))
REPRESENTATION_ITEM('')
);
#130=(
BOUNDED_CURVE()
B_SPLINE_CURVE(2,(#5056,#5057,#5058),.UNSPECIFIED.,.F.,.F.)
B_SPLINE_CURVE_WITH_KNOTS((3,3),(2.47778215640188,3.41264239816114),
 .UNSPECIFIED.)
CURVE()
GEOMETRIC_REPRESENTATION_ITEM()
RATIONAL_B_SPLINE_CURVE((2.01757984944671,2.01757984944671,1.87272413359279))
REPRESENTATION_ITEM('')
);
#131=(
BOUNDED_CURVE()
B_SPLINE_CURVE(2,(#5062,#5063,#5064),.UNSPECIFIED.,.F.,.F.)
B_SPLINE_CURVE_WITH_KNOTS((3,3),(-2.47778215640188,-1.54292191464263),
 .UNSPECIFIED.)
CURVE()
GEOMETRIC_REPRESENTATION_ITEM()
RATIONAL_B_SPLINE_CURVE((2.01757984944671,2.01757984944671,1.87272413359279))
REPRESENTATION_ITEM('')
);
#132=(
BOUNDED_CURVE()
B_SPLINE_CURVE(2,(#5065,#5066,#5067),.UNSPECIFIED.,.F.,.F.)
B_SPLINE_CURVE_WITH_KNOTS((3,3),(-3.41264239816112,-2.47778215640188),
 .UNSPECIFIED.)
CURVE()
GEOMETRIC_REPRESENTATION_ITEM()
RATIONAL_B_SPLINE_CURVE((1.8727241335928,2.01757984944671,2.01757984944671))
REPRESENTATION_ITEM('')
);
#133=(
BOUNDED_CURVE()
B_SPLINE_CURVE(2,(#5070,#5071,#5072),.UNSPECIFIED.,.F.,.F.)
B_SPLINE_CURVE_WITH_KNOTS((3,3),(1.54292191464265,2.47778215640188),
 .UNSPECIFIED.)
CURVE()
GEOMETRIC_REPRESENTATION_ITEM()
RATIONAL_B_SPLINE_CURVE((1.8727241335928,2.01757984944671,2.01757984944671))
REPRESENTATION_ITEM('')
);
#134=(
BOUNDED_CURVE()
B_SPLINE_CURVE(2,(#5074,#5075,#5076),.UNSPECIFIED.,.F.,.F.)
B_SPLINE_CURVE_WITH_KNOTS((3,3),(2.47778215640188,3.41264239816112),
 .UNSPECIFIED.)
CURVE()
GEOMETRIC_REPRESENTATION_ITEM()
RATIONAL_B_SPLINE_CURVE((2.01757984944671,2.01757984944671,1.8727241335928))
REPRESENTATION_ITEM('')
);
#135=(
BOUNDED_CURVE()
B_SPLINE_CURVE(2,(#5080,#5081,#5082),.UNSPECIFIED.,.F.,.F.)
B_SPLINE_CURVE_WITH_KNOTS((3,3),(-2.47778215640189,-1.54292191464265),
 .UNSPECIFIED.)
CURVE()
GEOMETRIC_REPRESENTATION_ITEM()
RATIONAL_B_SPLINE_CURVE((2.0175798494467,2.01757984944671,1.8727241335928))
REPRESENTATION_ITEM('')
);
#136=(
BOUNDED_CURVE()
B_SPLINE_CURVE(2,(#5083,#5084,#5085),.UNSPECIFIED.,.F.,.F.)
B_SPLINE_CURVE_WITH_KNOTS((3,3),(-3.41264239816112,-2.47778215640189),
 .UNSPECIFIED.)
CURVE()
GEOMETRIC_REPRESENTATION_ITEM()
RATIONAL_B_SPLINE_CURVE((1.8727241335928,2.0175798494467,2.0175798494467))
REPRESENTATION_ITEM('')
);
#137=(
BOUNDED_CURVE()
B_SPLINE_CURVE(2,(#5088,#5089,#5090),.UNSPECIFIED.,.F.,.F.)
B_SPLINE_CURVE_WITH_KNOTS((3,3),(1.54292191464263,2.47778215640189),
 .UNSPECIFIED.)
CURVE()
GEOMETRIC_REPRESENTATION_ITEM()
RATIONAL_B_SPLINE_CURVE((1.8727241335928,2.01757984944671,2.01757984944671))
REPRESENTATION_ITEM('')
);
#138=(
BOUNDED_CURVE()
B_SPLINE_CURVE(2,(#5091,#5092,#5093),.UNSPECIFIED.,.F.,.F.)
B_SPLINE_CURVE_WITH_KNOTS((3,3),(2.47778215640189,3.41264239816113),
 .UNSPECIFIED.)
CURVE()
GEOMETRIC_REPRESENTATION_ITEM()
RATIONAL_B_SPLINE_CURVE((2.01757984944671,2.01757984944671,1.8727241335928))
REPRESENTATION_ITEM('')
);
#139=(
BOUNDED_CURVE()
B_SPLINE_CURVE(2,(#5095,#5096,#5097),.UNSPECIFIED.,.F.,.F.)
B_SPLINE_CURVE_WITH_KNOTS((3,3),(-2.47778215640189,-1.54292191464264),
 .UNSPECIFIED.)
CURVE()
GEOMETRIC_REPRESENTATION_ITEM()
RATIONAL_B_SPLINE_CURVE((2.01757984944671,2.01757984944672,1.8727241335928))
REPRESENTATION_ITEM('')
);
#140=(
BOUNDED_CURVE()
B_SPLINE_CURVE(2,(#5098,#5099,#5100),.UNSPECIFIED.,.F.,.F.)
B_SPLINE_CURVE_WITH_KNOTS((3,3),(-3.41264239816114,-2.47778215640189),
 .UNSPECIFIED.)
CURVE()
GEOMETRIC_REPRESENTATION_ITEM()
RATIONAL_B_SPLINE_CURVE((1.8727241335928,2.01757984944671,2.01757984944671))
REPRESENTATION_ITEM('')
);
#180=SHAPE_REPRESENTATION_RELATIONSHIP('SRR','None',#5710,#191);
#191=ADVANCED_BREP_SHAPE_REPRESENTATION('',(#213),#5651);
#202=STYLED_ITEM('',(#5770),#213);
#213=MANIFOLD_SOLID_BREP('Body1',#3064);
#252=CYLINDRICAL_SURFACE('',#3326,5.);
#307=FACE_BOUND('',#628,.T.);
#308=FACE_BOUND('',#630,.T.);
#402=FACE_OUTER_BOUND('',#620,.T.);
#403=FACE_OUTER_BOUND('',#621,.T.);
#404=FACE_OUTER_BOUND('',#622,.T.);
#405=FACE_OUTER_BOUND('',#623,.T.);
#406=FACE_OUTER_BOUND('',#624,.T.);
#407=FACE_OUTER_BOUND('',#625,.T.);
#408=FACE_OUTER_BOUND('',#626,.T.);
#409=FACE_OUTER_BOUND('',#627,.T.);
#410=FACE_OUTER_BOUND('',#629,.T.);
#411=FACE_OUTER_BOUND('',#631,.T.);
#412=FACE_OUTER_BOUND('',#632,.T.);
#413=FACE_OUTER_BOUND('',#633,.T.);
#414=FACE_OUTER_BOUND('',#634,.T.);
#415=FACE_OUTER_BOUND('',#635,.T.);
#416=FACE_OUTER_BOUND('',#636,.T.);
#417=FACE_OUTER_BOUND('',#637,.T.);
#418=FACE_OUTER_BOUND('',#638,.T.);
#419=FACE_OUTER_BOUND('',#639,.T.);
#420=FACE_OUTER_BOUND('',#640,.T.);
#421=FACE_OUTER_BOUND('',#641,.T.);
#422=FACE_OUTER_BOUND('',#642,.T.);
#620=EDGE_LOOP('',(#2280,#2281,#2282,#2283));
#621=EDGE_LOOP('',(#2284,#2285,#2286,#2287,#2288,#2289));
#622=EDGE_LOOP('',(#2290,#2291,#2292,#2293,#2294,#2295));
#623=EDGE_LOOP('',(#2296,#2297,#2298,#2299,#2300,#2301));
#624=EDGE_LOOP('',(#2302,#2303,#2304,#2305,#2306,#2307));
#625=EDGE_LOOP('',(#2308,#2309,#2310,#2311,#2312,#2313));
#626=EDGE_LOOP('',(#2314,#2315,#2316,#2317,#2318,#2319));
#627=EDGE_LOOP('',(#2320,#2321,#2322,#2323,#2324,#2325));
#628=EDGE_LOOP('',(#2326));
#629=EDGE_LOOP('',(#2327,#2328,#2329,#2330,#2331,#2332));
#630=EDGE_LOOP('',(#2333));
#631=EDGE_LOOP('',(#2334,#2335,#2336));
#632=EDGE_LOOP('',(#2337,#2338,#2339));
#633=EDGE_LOOP('',(#2340,#2341,#2342));
#634=EDGE_LOOP('',(#2343,#2344,#2345));
#635=EDGE_LOOP('',(#2346,#2347,#2348));
#636=EDGE_LOOP('',(#2349,#2350,#2351));
#637=EDGE_LOOP('',(#2352,#2353,#2354));
#638=EDGE_LOOP('',(#2355,#2356,#2357));
#639=EDGE_LOOP('',(#2358,#2359,#2360));
#640=EDGE_LOOP('',(#2361,#2362,#2363));
#641=EDGE_LOOP('',(#2364,#2365,#2366));
#642=EDGE_LOOP('',(#2367,#2368,#2369));
#850=LINE('',#4991,#1046);
#851=LINE('',#4996,#1047);
#852=LINE('',#5006,#1048);
#853=LINE('',#5024,#1049);
#854=LINE('',#5039,#1050);
#855=LINE('',#5060,#1051);
#856=LINE('',#5078,#1052);
#1046=VECTOR('',#3912,5.);
#1047=VECTOR('',#3917,1000.);
#1048=VECTOR('',#3918,1000.);
#1049=VECTOR('',#3921,1000.);
#1050=VECTOR('',#3924,1000.);
#1051=VECTOR('',#3927,1000.);
#1052=VECTOR('',#3930,1000.);
#1222=CIRCLE('',#3327,5.);
#1223=CIRCLE('',#3328,4.99999999999999);
#1224=CIRCLE('',#3336,8.);
#1225=CIRCLE('',#3337,8.);
#1226=CIRCLE('',#3338,8.);
#1227=CIRCLE('',#3339,8.);
#1228=CIRCLE('',#3340,8.);
#1229=CIRCLE('',#3341,8.);
#1230=CIRCLE('',#3343,8.);
#1231=CIRCLE('',#3344,8.);
#1232=CIRCLE('',#3345,8.);
#1233=CIRCLE('',#3346,8.);
#1234=CIRCLE('',#3347,8.);
#1235=CIRCLE('',#3348,8.);
#1415=VERTEX_POINT('',#4988);
#1416=VERTEX_POINT('',#4990);
#1417=VERTEX_POINT('',#4994);
#1418=VERTEX_POINT('',#4995);
#1419=VERTEX_POINT('',#4997);
#1420=VERTEX_POINT('',#5001);
#1421=VERTEX_POINT('',#5005);
#1422=VERTEX_POINT('',#5007);
#1423=VERTEX_POINT('',#5015);
#1424=VERTEX_POINT('',#5019);
#1425=VERTEX_POINT('',#5023);
#1426=VERTEX_POINT('',#5025);
#1427=VERTEX_POINT('',#5033);
#1428=VERTEX_POINT('',#5034);
#1429=VERTEX_POINT('',#5038);
#1430=VERTEX_POINT('',#5040);
#1431=VERTEX_POINT('',#5051);
#1432=VERTEX_POINT('',#5055);
#1433=VERTEX_POINT('',#5059);
#1434=VERTEX_POINT('',#5061);
#1435=VERTEX_POINT('',#5069);
#1436=VERTEX_POINT('',#5073);
#1437=VERTEX_POINT('',#5077);
#1438=VERTEX_POINT('',#5079);
#1439=VERTEX_POINT('',#5087);
#1440=VERTEX_POINT('',#5094);
#1723=EDGE_CURVE('',#1415,#1415,#1222,.T.);
#1724=EDGE_CURVE('',#1415,#1416,#850,.T.);
#1725=EDGE_CURVE('',#1416,#1416,#1223,.T.);
#1726=EDGE_CURVE('',#1417,#1418,#851,.T.);
#1727=EDGE_CURVE('',#1418,#1419,#117,.T.);
#1728=EDGE_CURVE('',#1419,#1420,#118,.T.);
#1729=EDGE_CURVE('',#1421,#1420,#852,.T.);
#1730=EDGE_CURVE('',#1422,#1421,#119,.T.);
#1731=EDGE_CURVE('',#1417,#1422,#120,.T.);
#1732=EDGE_CURVE('',#1420,#1423,#121,.T.);
#1733=EDGE_CURVE('',#1423,#1424,#122,.T.);
#1734=EDGE_CURVE('',#1425,#1424,#853,.T.);
#1735=EDGE_CURVE('',#1426,#1425,#123,.T.);
#1736=EDGE_CURVE('',#1421,#1426,#124,.T.);
#1737=EDGE_CURVE('',#1427,#1428,#125,.T.);
#1738=EDGE_CURVE('',#1429,#1427,#854,.T.);
#1739=EDGE_CURVE('',#1429,#1430,#126,.T.);
#1740=EDGE_CURVE('',#1430,#1425,#127,.T.);
#1741=EDGE_CURVE('',#1428,#1424,#128,.T.);
#1742=EDGE_CURVE('',#1427,#1431,#129,.T.);
#1743=EDGE_CURVE('',#1431,#1432,#130,.T.);
#1744=EDGE_CURVE('',#1433,#1432,#855,.T.);
#1745=EDGE_CURVE('',#1434,#1433,#131,.T.);
#1746=EDGE_CURVE('',#1429,#1434,#132,.T.);
#1747=EDGE_CURVE('',#1432,#1435,#133,.T.);
#1748=EDGE_CURVE('',#1435,#1436,#134,.T.);
#1749=EDGE_CURVE('',#1437,#1436,#856,.T.);
#1750=EDGE_CURVE('',#1438,#1437,#135,.T.);
#1751=EDGE_CURVE('',#1433,#1438,#136,.T.);
#1752=EDGE_CURVE('',#1436,#1439,#137,.T.);
#1753=EDGE_CURVE('',#1439,#1418,#138,.T.);
#1754=EDGE_CURVE('',#1440,#1417,#139,.T.);
#1755=EDGE_CURVE('',#1437,#1440,#140,.T.);
#1756=EDGE_CURVE('',#1439,#1419,#1224,.T.);
#1757=EDGE_CURVE('',#1435,#1439,#1225,.T.);
#1758=EDGE_CURVE('',#1431,#1435,#1226,.T.);
#1759=EDGE_CURVE('',#1428,#1431,#1227,.T.);
#1760=EDGE_CURVE('',#1428,#1423,#1228,.T.);
#1761=EDGE_CURVE('',#1419,#1423,#1229,.T.);
#1762=EDGE_CURVE('',#1440,#1438,#1230,.T.);
#1763=EDGE_CURVE('',#1422,#1440,#1231,.T.);
#1764=EDGE_CURVE('',#1426,#1422,#1232,.T.);
#1765=EDGE_CURVE('',#1430,#1426,#1233,.T.);
#1766=EDGE_CURVE('',#1434,#1430,#1234,.T.);
#1767=EDGE_CURVE('',#1438,#1434,#1235,.T.);
#2280=ORIENTED_EDGE('',*,*,#1723,.F.);
#2281=ORIENTED_EDGE('',*,*,#1724,.T.);
#2282=ORIENTED_EDGE('',*,*,#1725,.T.);
#2283=ORIENTED_EDGE('',*,*,#1724,.F.);
#2284=ORIENTED_EDGE('',*,*,#1726,.T.);
#2285=ORIENTED_EDGE('',*,*,#1727,.T.);
#2286=ORIENTED_EDGE('',*,*,#1728,.T.);
#2287=ORIENTED_EDGE('',*,*,#1729,.F.);
#2288=ORIENTED_EDGE('',*,*,#1730,.F.);
#2289=ORIENTED_EDGE('',*,*,#1731,.F.);
#2290=ORIENTED_EDGE('',*,*,#1729,.T.);
#2291=ORIENTED_EDGE('',*,*,#1732,.T.);
#2292=ORIENTED_EDGE('',*,*,#1733,.T.);
#2293=ORIENTED_EDGE('',*,*,#1734,.F.);
#2294=ORIENTED_EDGE('',*,*,#1735,.F.);
#2295=ORIENTED_EDGE('',*,*,#1736,.F.);
#2296=ORIENTED_EDGE('',*,*,#1737,.F.);
#2297=ORIENTED_EDGE('',*,*,#1738,.F.);
#2298=ORIENTED_EDGE('',*,*,#1739,.T.);
#2299=ORIENTED_EDGE('',*,*,#1740,.T.);
#2300=ORIENTED_EDGE('',*,*,#1734,.T.);
#2301=ORIENTED_EDGE('',*,*,#1741,.F.);
#2302=ORIENTED_EDGE('',*,*,#1738,.T.);
#2303=ORIENTED_EDGE('',*,*,#1742,.T.);
#2304=ORIENTED_EDGE('',*,*,#1743,.T.);
#2305=ORIENTED_EDGE('',*,*,#1744,.F.);
#2306=ORIENTED_EDGE('',*,*,#1745,.F.);
#2307=ORIENTED_EDGE('',*,*,#1746,.F.);
#2308=ORIENTED_EDGE('',*,*,#1744,.T.);
#2309=ORIENTED_EDGE('',*,*,#1747,.T.);
#2310=ORIENTED_EDGE('',*,*,#1748,.T.);
#2311=ORIENTED_EDGE('',*,*,#1749,.F.);
#2312=ORIENTED_EDGE('',*,*,#1750,.F.);
#2313=ORIENTED_EDGE('',*,*,#1751,.F.);
#2314=ORIENTED_EDGE('',*,*,#1749,.T.);
#2315=ORIENTED_EDGE('',*,*,#1752,.T.);
#2316=ORIENTED_EDGE('',*,*,#1753,.T.);
#2317=ORIENTED_EDGE('',*,*,#1726,.F.);
#2318=ORIENTED_EDGE('',*,*,#1754,.F.);
#2319=ORIENTED_EDGE('',*,*,#1755,.F.);
#2320=ORIENTED_EDGE('',*,*,#1756,.F.);
#2321=ORIENTED_EDGE('',*,*,#1757,.F.);
#2322=ORIENTED_EDGE('',*,*,#1758,.F.);
#2323=ORIENTED_EDGE('',*,*,#1759,.F.);
#2324=ORIENTED_EDGE('',*,*,#1760,.T.);
#2325=ORIENTED_EDGE('',*,*,#1761,.F.);
#2326=ORIENTED_EDGE('',*,*,#1725,.F.);
#2327=ORIENTED_EDGE('',*,*,#1762,.F.);
#2328=ORIENTED_EDGE('',*,*,#1763,.F.);
#2329=ORIENTED_EDGE('',*,*,#1764,.F.);
#2330=ORIENTED_EDGE('',*,*,#1765,.F.);
#2331=ORIENTED_EDGE('',*,*,#1766,.F.);
#2332=ORIENTED_EDGE('',*,*,#1767,.F.);
#2333=ORIENTED_EDGE('',*,*,#1723,.T.);
#2334=ORIENTED_EDGE('',*,*,#1731,.T.);
#2335=ORIENTED_EDGE('',*,*,#1763,.T.);
#2336=ORIENTED_EDGE('',*,*,#1754,.T.);
#2337=ORIENTED_EDGE('',*,*,#1730,.T.);
#2338=ORIENTED_EDGE('',*,*,#1736,.T.);
#2339=ORIENTED_EDGE('',*,*,#1764,.T.);
#2340=ORIENTED_EDGE('',*,*,#1735,.T.);
#2341=ORIENTED_EDGE('',*,*,#1740,.F.);
#2342=ORIENTED_EDGE('',*,*,#1765,.T.);
#2343=ORIENTED_EDGE('',*,*,#1746,.T.);
#2344=ORIENTED_EDGE('',*,*,#1766,.T.);
#2345=ORIENTED_EDGE('',*,*,#1739,.F.);
#2346=ORIENTED_EDGE('',*,*,#1745,.T.);
#2347=ORIENTED_EDGE('',*,*,#1751,.T.);
#2348=ORIENTED_EDGE('',*,*,#1767,.T.);
#2349=ORIENTED_EDGE('',*,*,#1750,.T.);
#2350=ORIENTED_EDGE('',*,*,#1755,.T.);
#2351=ORIENTED_EDGE('',*,*,#1762,.T.);
#2352=ORIENTED_EDGE('',*,*,#1757,.T.);
#2353=ORIENTED_EDGE('',*,*,#1752,.F.);
#2354=ORIENTED_EDGE('',*,*,#1748,.F.);
#2355=ORIENTED_EDGE('',*,*,#1758,.T.);
#2356=ORIENTED_EDGE('',*,*,#1747,.F.);
#2357=ORIENTED_EDGE('',*,*,#1743,.F.);
#2358=ORIENTED_EDGE('',*,*,#1737,.T.);
#2359=ORIENTED_EDGE('',*,*,#1759,.T.);
#2360=ORIENTED_EDGE('',*,*,#1742,.F.);
#2361=ORIENTED_EDGE('',*,*,#1760,.F.);
#2362=ORIENTED_EDGE('',*,*,#1741,.T.);
#2363=ORIENTED_EDGE('',*,*,#1733,.F.);
#2364=ORIENTED_EDGE('',*,*,#1761,.T.);
#2365=ORIENTED_EDGE('',*,*,#1732,.F.);
#2366=ORIENTED_EDGE('',*,*,#1728,.F.);
#2367=ORIENTED_EDGE('',*,*,#1753,.F.);
#2368=ORIENTED_EDGE('',*,*,#1756,.T.);
#2369=ORIENTED_EDGE('',*,*,#1727,.F.);
#2816=PLANE('',#3329);
#2817=PLANE('',#3330);
#2818=PLANE('',#3331);
#2819=PLANE('',#3332);
#2820=PLANE('',#3333);
#2821=PLANE('',#3334);
#2822=PLANE('',#3335);
#2823=PLANE('',#3342);
#2943=ADVANCED_FACE('',(#402),#252,.F.);
#2944=ADVANCED_FACE('',(#403),#2816,.T.);
#2945=ADVANCED_FACE('',(#404),#2817,.T.);
#2946=ADVANCED_FACE('',(#405),#2818,.F.);
#2947=ADVANCED_FACE('',(#406),#2819,.T.);
#2948=ADVANCED_FACE('',(#407),#2820,.T.);
#2949=ADVANCED_FACE('',(#408),#2821,.T.);
#2950=ADVANCED_FACE('',(#409,#307),#2822,.F.);
#2951=ADVANCED_FACE('',(#410,#308),#2823,.T.);
#2952=ADVANCED_FACE('',(#411),#83,.T.);
#2953=ADVANCED_FACE('',(#412),#84,.T.);
#2954=ADVANCED_FACE('',(#413),#85,.T.);
#2955=ADVANCED_FACE('',(#414),#86,.T.);
#2956=ADVANCED_FACE('',(#415),#87,.T.);
#2957=ADVANCED_FACE('',(#416),#88,.T.);
#2958=ADVANCED_FACE('',(#417),#89,.T.);
#2959=ADVANCED_FACE('',(#418),#90,.T.);
#2960=ADVANCED_FACE('',(#419),#91,.T.);
#2961=ADVANCED_FACE('',(#420),#92,.T.);
#2962=ADVANCED_FACE('',(#421),#93,.T.);
#2963=ADVANCED_FACE('',(#422),#94,.T.);
#3064=CLOSED_SHELL('',(#2943,#2944,#2945,#2946,#2947,#2948,#2949,#2950,
#2951,#2952,#2953,#2954,#2955,#2956,#2957,#2958,#2959,#2960,#2961,#2962,
#2963));
#3325=AXIS2_PLACEMENT_3D('',#4986,#3906,#3907);
#3326=AXIS2_PLACEMENT_3D('',#4987,#3908,#3909);
#3327=AXIS2_PLACEMENT_3D('',#4989,#3910,#3911);
#3328=AXIS2_PLACEMENT_3D('',#4992,#3913,#3914);
#3329=AXIS2_PLACEMENT_3D('',#4993,#3915,#3916);
#3330=AXIS2_PLACEMENT_3D('',#5014,#3919,#3920);
#3331=AXIS2_PLACEMENT_3D('',#5032,#3922,#3923);
#3332=AXIS2_PLACEMENT_3D('',#5050,#3925,#3926);
#3333=AXIS2_PLACEMENT_3D('',#5068,#3928,#3929);
#3334=AXIS2_PLACEMENT_3D('',#5086,#3931,#3932);
#3335=AXIS2_PLACEMENT_3D('',#5101,#3933,#3934);
#3336=AXIS2_PLACEMENT_3D('',#5102,#3935,#3936);
#3337=AXIS2_PLACEMENT_3D('',#5103,#3937,#3938);
#3338=AXIS2_PLACEMENT_3D('',#5104,#3939,#3940);
#3339=AXIS2_PLACEMENT_3D('',#5105,#3941,#3942);
#3340=AXIS2_PLACEMENT_3D('',#5106,#3943,#3944);
#3341=AXIS2_PLACEMENT_3D('',#5107,#3945,#3946);
#3342=AXIS2_PLACEMENT_3D('',#5108,#3947,#3948);
#3343=AXIS2_PLACEMENT_3D('',#5109,#3949,#3950);
#3344=AXIS2_PLACEMENT_3D('',#5110,#3951,#3952);
#3345=AXIS2_PLACEMENT_3D('',#5111,#3953,#3954);
#3346=AXIS2_PLACEMENT_3D('',#5112,#3955,#3956);
#3347=AXIS2_PLACEMENT_3D('',#5113,#3957,#3958);
#3348=AXIS2_PLACEMENT_3D('',#5114,#3959,#3960);
#3349=AXIS2_PLACEMENT_3D('',#5115,#3961,#3962);
#3350=AXIS2_PLACEMENT_3D('',#5116,#3963,#3964);
#3351=AXIS2_PLACEMENT_3D('',#5117,#3965,#3966);
#3352=AXIS2_PLACEMENT_3D('',#5118,#3967,#3968);
#3353=AXIS2_PLACEMENT_3D('',#5119,#3969,#3970);
#3354=AXIS2_PLACEMENT_3D('',#5120,#3971,#3972);
#3355=AXIS2_PLACEMENT_3D('',#5121,#3973,#3974);
#3356=AXIS2_PLACEMENT_3D('',#5122,#3975,#3976);
#3357=AXIS2_PLACEMENT_3D('',#5123,#3977,#3978);
#3358=AXIS2_PLACEMENT_3D('',#5124,#3979,#3980);
#3359=AXIS2_PLACEMENT_3D('',#5125,#3981,#3982);
#3360=AXIS2_PLACEMENT_3D('',#5126,#3983,#3984);
#3906=DIRECTION('axis',(0.,0.,1.));
#3907=DIRECTION('refdir',(1.,0.,0.));
#3908=DIRECTION('center_axis',(0.,0.,1.));
#3909=DIRECTION('ref_axis',(1.,0.,0.));
#3910=DIRECTION('center_axis',(0.,0.,1.));
#3911=DIRECTION('ref_axis',(-1.,0.,0.));
#3912=DIRECTION('',(0.,0.,1.));
#3913=DIRECTION('center_axis',(0.,0.,1.));
#3914=DIRECTION('ref_axis',(1.,0.,0.));
#3915=DIRECTION('center_axis',(-0.500000000000003,0.866025403784437,0.));
#3916=DIRECTION('ref_axis',(-0.866025403784437,-0.500000000000003,0.));
#3917=DIRECTION('',(0.,0.,1.));
#3918=DIRECTION('',(0.,0.,1.));
#3919=DIRECTION('center_axis',(0.500000000000004,0.866025403784437,0.));
#3920=DIRECTION('ref_axis',(-0.866025403784437,0.500000000000004,0.));
#3921=DIRECTION('',(0.,0.,1.));
#3922=DIRECTION('center_axis',(-1.,0.,0.));
#3923=DIRECTION('ref_axis',(0.,0.,1.));
#3924=DIRECTION('',(0.,0.,1.));
#3925=DIRECTION('center_axis',(0.500000000000002,-0.866025403784437,0.));
#3926=DIRECTION('ref_axis',(0.866025403784437,0.500000000000002,0.));
#3927=DIRECTION('',(0.,0.,1.));
#3928=DIRECTION('center_axis',(-0.500000000000003,-0.866025403784437,0.));
#3929=DIRECTION('ref_axis',(0.866025403784437,-0.500000000000003,0.));
#3930=DIRECTION('',(0.,0.,1.));
#3931=DIRECTION('center_axis',(-1.,0.,0.));
#3932=DIRECTION('ref_axis',(0.,0.,1.));
#3933=DIRECTION('center_axis',(0.,0.,-1.));
#3934=DIRECTION('ref_axis',(-1.,0.,0.));
#3935=DIRECTION('center_axis',(0.,0.,-1.));
#3936=DIRECTION('ref_axis',(-1.,0.,0.));
#3937=DIRECTION('center_axis',(0.,0.,-1.));
#3938=DIRECTION('ref_axis',(-1.,0.,0.));
#3939=DIRECTION('center_axis',(0.,0.,-1.));
#3940=DIRECTION('ref_axis',(-1.,0.,0.));
#3941=DIRECTION('center_axis',(0.,0.,-1.));
#3942=DIRECTION('ref_axis',(-1.,0.,0.));
#3943=DIRECTION('center_axis',(0.,0.,1.));
#3944=DIRECTION('ref_axis',(1.,0.,0.));
#3945=DIRECTION('center_axis',(0.,0.,-1.));
#3946=DIRECTION('ref_axis',(-1.,0.,0.));
#3947=DIRECTION('center_axis',(0.,0.,-1.));
#3948=DIRECTION('ref_axis',(-1.,0.,0.));
#3949=DIRECTION('center_axis',(0.,0.,1.));
#3950=DIRECTION('ref_axis',(-1.,0.,0.));
#3951=DIRECTION('center_axis',(0.,0.,1.));
#3952=DIRECTION('ref_axis',(-1.,-3.5527136788005E-15,0.));
#3953=DIRECTION('center_axis',(0.,0.,1.));
#3954=DIRECTION('ref_axis',(-1.,0.,0.));
#3955=DIRECTION('center_axis',(0.,0.,1.));
#3956=DIRECTION('ref_axis',(1.,0.,0.));
#3957=DIRECTION('center_axis',(0.,0.,1.));
#3958=DIRECTION('ref_axis',(-1.,1.77635683940025E-15,0.));
#3959=DIRECTION('center_axis',(0.,0.,1.));
#3960=DIRECTION('ref_axis',(-1.,0.,0.));
#3961=DIRECTION('center_axis',(0.,0.,1.));
#3962=DIRECTION('ref_axis',(1.,0.,0.));
#3963=DIRECTION('center_axis',(0.,0.,1.));
#3964=DIRECTION('ref_axis',(1.,0.,0.));
#3965=DIRECTION('center_axis',(0.,0.,1.));
#3966=DIRECTION('ref_axis',(1.,0.,0.));
#3967=DIRECTION('center_axis',(0.,0.,1.));
#3968=DIRECTION('ref_axis',(1.,0.,0.));
#3969=DIRECTION('center_axis',(0.,0.,1.));
#3970=DIRECTION('ref_axis',(1.,0.,0.));
#3971=DIRECTION('center_axis',(0.,0.,1.));
#3972=DIRECTION('ref_axis',(1.,0.,0.));
#3973=DIRECTION('center_axis',(0.,0.,-1.));
#3974=DIRECTION('ref_axis',(-1.,0.,0.));
#3975=DIRECTION('center_axis',(0.,0.,-1.));
#3976=DIRECTION('ref_axis',(-1.,0.,0.));
#3977=DIRECTION('center_axis',(0.,0.,-1.));
#3978=DIRECTION('ref_axis',(-1.,0.,0.));
#3979=DIRECTION('center_axis',(0.,0.,-1.));
#3980=DIRECTION('ref_axis',(-1.,0.,0.));
#3981=DIRECTION('center_axis',(0.,0.,-1.));
#3982=DIRECTION('ref_axis',(-1.,0.,0.));
#3983=DIRECTION('center_axis',(0.,0.,-1.));
#3984=DIRECTION('ref_axis',(-1.,0.,0.));
#4986=CARTESIAN_POINT('',(0.,0.,0.));
#4987=CARTESIAN_POINT('Origin',(0.,0.,-25.0375057290932));
#4988=CARTESIAN_POINT('',(-5.,-6.12323399573677E-16,-8.4));
#4989=CARTESIAN_POINT('Origin',(0.,0.,-8.4));
#4990=CARTESIAN_POINT('',(-5.,-6.12323399573677E-16,0.));
#4991=CARTESIAN_POINT('',(-5.,-6.12323399573677E-16,-25.0375057290932));
#4992=CARTESIAN_POINT('Origin',(0.,0.,-3.25260651745651E-16));
#4993=CARTESIAN_POINT('Origin',(1.58955611655707E-15,9.23760430703403,-8.4));
#4994=CARTESIAN_POINT('',(-8.,4.61880215351705,-7.68546882018366));
#4995=CARTESIAN_POINT('',(-8.,4.61880215351699,-0.714531179816323));
#4996=CARTESIAN_POINT('',(-8.,4.61880215351699,-8.4));
#4997=CARTESIAN_POINT('',(-4.00000000000002,6.9282032302755,0.));
#4998=CARTESIAN_POINT('Ctrl Pts',(-8.00000000003847,4.61880215349478,-0.714531179829145));
#4999=CARTESIAN_POINT('Ctrl Pts',(-5.85640646056649,5.85640646054208,-8.88178419700125E-16));
#5000=CARTESIAN_POINT('Ctrl Pts',(-4.00000000000002,6.9282032302755,-8.80439423444571E-16));
#5001=CARTESIAN_POINT('',(-2.60208521396521E-15,9.23760430703403,-0.71453117981634));
#5002=CARTESIAN_POINT('Ctrl Pts',(-4.00000000000002,6.9282032302755,-8.80439423444571E-16));
#5003=CARTESIAN_POINT('Ctrl Pts',(-2.14359353943353,8.00000000000893,-8.83359324974957E-16));
#5004=CARTESIAN_POINT('Ctrl Pts',(3.84704779639695E-11,9.23760430705624,
-0.714531179829162));
#5005=CARTESIAN_POINT('',(8.67361737988404E-16,9.23760430703403,-7.68546882018366));
#5006=CARTESIAN_POINT('',(1.58955611655707E-15,9.23760430703403,-8.4));
#5007=CARTESIAN_POINT('',(-4.00000000000002,6.9282032302755,-8.4));
#5008=CARTESIAN_POINT('Ctrl Pts',(-4.00000000000004,6.92820323027549,-8.4));
#5009=CARTESIAN_POINT('Ctrl Pts',(-2.14359353943354,8.00000000000893,-8.4));
#5010=CARTESIAN_POINT('Ctrl Pts',(3.84766434846935E-11,9.23760430705625,
-7.68546882017083));
#5011=CARTESIAN_POINT('Ctrl Pts',(-8.00000000003847,4.61880215349478,-7.68546882017085));
#5012=CARTESIAN_POINT('Ctrl Pts',(-5.8564064605665,5.85640646054207,-8.4));
#5013=CARTESIAN_POINT('Ctrl Pts',(-4.00000000000004,6.92820323027549,-8.4));
#5014=CARTESIAN_POINT('Origin',(8.,4.61880215351698,-8.4));
#5015=CARTESIAN_POINT('',(4.00000000000003,6.92820323027549,0.));
#5016=CARTESIAN_POINT('Ctrl Pts',(-3.84662095265451E-11,9.23760430705625,
-0.714531179829163));
#5017=CARTESIAN_POINT('Ctrl Pts',(2.14359353943354,8.00000000000893,-6.66133814775094E-16));
#5018=CARTESIAN_POINT('Ctrl Pts',(4.00000000000003,6.9282032302755,-1.10054927930571E-15));
#5019=CARTESIAN_POINT('',(8.,4.61880215351705,-0.71453117981634));
#5020=CARTESIAN_POINT('Ctrl Pts',(4.00000000000003,6.9282032302755,-1.10054927930571E-15));
#5021=CARTESIAN_POINT('Ctrl Pts',(5.85640646056649,5.85640646054208,-1.85819040300646E-15));
#5022=CARTESIAN_POINT('Ctrl Pts',(8.00000000003845,4.61880215349479,-0.71453117982914));
#5023=CARTESIAN_POINT('',(8.,4.61880215351705,-7.68546882018366));
#5024=CARTESIAN_POINT('',(8.,4.61880215351698,-8.4));
#5025=CARTESIAN_POINT('',(4.00000000000003,6.92820323027549,-8.4));
#5026=CARTESIAN_POINT('Ctrl Pts',(4.00000000000004,6.92820323027549,-8.4));
#5027=CARTESIAN_POINT('Ctrl Pts',(5.85640646056649,5.85640646054208,-8.4));
#5028=CARTESIAN_POINT('Ctrl Pts',(8.00000000003844,4.61880215349479,-7.68546882017086));
#5029=CARTESIAN_POINT('Ctrl Pts',(-3.84676323390199E-11,9.23760430705624,
-7.68546882017084));
#5030=CARTESIAN_POINT('Ctrl Pts',(2.14359353943355,8.00000000000892,-8.4));
#5031=CARTESIAN_POINT('Ctrl Pts',(4.00000000000004,6.92820323027549,-8.4));
#5032=CARTESIAN_POINT('Origin',(8.,4.61880215351698,-8.4));
#5033=CARTESIAN_POINT('',(8.,-4.61880215351705,-0.71453117981634));
#5034=CARTESIAN_POINT('',(8.,0.,0.));
#5035=CARTESIAN_POINT('Ctrl Pts',(8.00000000000001,-4.61880215356147,-0.714531179829163));
#5036=CARTESIAN_POINT('Ctrl Pts',(8.00000000000001,-2.14359353946685,-3.88578058618805E-16));
#5037=CARTESIAN_POINT('Ctrl Pts',(8.,4.40219711722286E-15,-8.80439423444572E-16));
#5038=CARTESIAN_POINT('',(8.,-4.61880215351705,-7.68546882018366));
#5039=CARTESIAN_POINT('',(8.,-4.61880215351705,-8.4));
#5040=CARTESIAN_POINT('',(8.,0.,-8.4));
#5041=CARTESIAN_POINT('Ctrl Pts',(8.,-4.61880215356146,-7.68546882017084));
#5042=CARTESIAN_POINT('Ctrl Pts',(8.,-2.14359353946686,-8.4));
#5043=CARTESIAN_POINT('Ctrl Pts',(8.,-1.49674701985577E-14,-8.4));
#5044=CARTESIAN_POINT('Ctrl Pts',(8.,-1.49674701985577E-14,-8.4));
#5045=CARTESIAN_POINT('Ctrl Pts',(8.,2.14359353946684,-8.4));
#5046=CARTESIAN_POINT('Ctrl Pts',(8.,4.61880215356146,-7.68546882017084));
#5047=CARTESIAN_POINT('Ctrl Pts',(8.,-7.04351538755657E-15,4.40219711722283E-16));
#5048=CARTESIAN_POINT('Ctrl Pts',(8.,2.14359353946685,1.78210854566576E-15));
#5049=CARTESIAN_POINT('Ctrl Pts',(8.,4.61880215356148,-0.714531179829165));
#5050=CARTESIAN_POINT('Origin',(-3.00462919747434E-15,-9.23760430703408,
-8.4));
#5051=CARTESIAN_POINT('',(4.00000000000002,-6.9282032302755,0.));
#5052=CARTESIAN_POINT('Ctrl Pts',(8.00000000003846,-4.61880215349484,-0.714531179829161));
#5053=CARTESIAN_POINT('Ctrl Pts',(5.85640646056651,-5.85640646054213,-2.80331313717852E-14));
#5054=CARTESIAN_POINT('Ctrl Pts',(4.00000000000005,-6.92820323027554,-2.72936221267818E-14));
#5055=CARTESIAN_POINT('',(-8.93382590128056E-14,-9.23760430703403,-0.71453117981634));
#5056=CARTESIAN_POINT('Ctrl Pts',(4.00000000000005,-6.92820323027554,-2.72936221267818E-14));
#5057=CARTESIAN_POINT('Ctrl Pts',(2.14359353943354,-8.00000000000898,-2.65463710222373E-14));
#5058=CARTESIAN_POINT('Ctrl Pts',(-3.84861289011922E-11,-9.2376043070563,
-0.714531179829196));
#5059=CARTESIAN_POINT('',(-8.93382590128056E-14,-9.23760430703403,-7.68546882018366));
#5060=CARTESIAN_POINT('',(-3.00462919747434E-15,-9.23760430703408,-8.4));
#5061=CARTESIAN_POINT('',(4.00000000000002,-6.9282032302755,-8.4));
#5062=CARTESIAN_POINT('Ctrl Pts',(4.00000000000004,-6.92820323027554,-8.39999999999997));
#5063=CARTESIAN_POINT('Ctrl Pts',(2.14359353943353,-8.00000000000898,-8.39999999999997));
#5064=CARTESIAN_POINT('Ctrl Pts',(-3.85013055675899E-11,-9.23760430705631,
-7.6854688201708));
#5065=CARTESIAN_POINT('Ctrl Pts',(8.00000000003848,-4.61880215349483,-7.68546882017083));
#5066=CARTESIAN_POINT('Ctrl Pts',(5.85640646056651,-5.85640646054213,-8.39999999999997));
#5067=CARTESIAN_POINT('Ctrl Pts',(4.00000000000004,-6.92820323027554,-8.39999999999997));
#5068=CARTESIAN_POINT('Origin',(-8.,-4.61880215351704,-8.4));
#5069=CARTESIAN_POINT('',(-4.00000000000003,-6.92820323027549,0.));
#5070=CARTESIAN_POINT('Ctrl Pts',(3.83779951531087E-11,-9.23760430705625,
-0.714531179829162));
#5071=CARTESIAN_POINT('Ctrl Pts',(-2.14359353943358,-8.00000000000896,-2.75890421619351E-14));
#5072=CARTESIAN_POINT('Ctrl Pts',(-4.00000000000004,-6.92820323027554,-2.72936221267818E-14));
#5073=CARTESIAN_POINT('',(-8.,-4.61880215351705,-0.71453117981634));
#5074=CARTESIAN_POINT('Ctrl Pts',(-4.00000000000004,-6.92820323027554,-2.72936221267818E-14));
#5075=CARTESIAN_POINT('Ctrl Pts',(-5.8564064605665,-5.85640646054213,-2.68814782430319E-14));
#5076=CARTESIAN_POINT('Ctrl Pts',(-8.00000000003846,-4.61880215349484,-0.714531179829158));
#5077=CARTESIAN_POINT('',(-8.,-4.61880215351705,-7.68546882018366));
#5078=CARTESIAN_POINT('',(-8.,-4.61880215351704,-8.4));
#5079=CARTESIAN_POINT('',(-4.00000000000003,-6.92820323027549,-8.4));
#5080=CARTESIAN_POINT('Ctrl Pts',(-4.00000000000003,-6.92820323027555,-8.39999999999998));
#5081=CARTESIAN_POINT('Ctrl Pts',(-5.8564064605665,-5.85640646054213,-8.39999999999998));
#5082=CARTESIAN_POINT('Ctrl Pts',(-8.00000000003846,-4.61880215349483,-7.68546882017084));
#5083=CARTESIAN_POINT('Ctrl Pts',(3.83836864030079E-11,-9.23760430705625,
-7.68546882017084));
#5084=CARTESIAN_POINT('Ctrl Pts',(-2.14359353943357,-8.00000000000896,-8.39999999999997));
#5085=CARTESIAN_POINT('Ctrl Pts',(-4.00000000000003,-6.92820323027555,-8.39999999999998));
#5086=CARTESIAN_POINT('Origin',(-8.,4.61880215351699,-8.4));
#5087=CARTESIAN_POINT('',(-8.,0.,0.));
#5088=CARTESIAN_POINT('Ctrl Pts',(-8.00000000000001,-4.61880215356147,-0.714531179829163));
#5089=CARTESIAN_POINT('Ctrl Pts',(-8.00000000000001,-2.14359353946685,-3.88578058618805E-16));
#5090=CARTESIAN_POINT('Ctrl Pts',(-8.,4.40219711722286E-15,-8.80439423444572E-16));
#5091=CARTESIAN_POINT('Ctrl Pts',(-8.,4.40219711722286E-15,-8.80439423444572E-16));
#5092=CARTESIAN_POINT('Ctrl Pts',(-8.,2.14359353946683,-1.72112737696137E-15));
#5093=CARTESIAN_POINT('Ctrl Pts',(-8.00000000000001,4.61880215356141,-0.714531179829147));
#5094=CARTESIAN_POINT('',(-8.,0.,-8.4));
#5095=CARTESIAN_POINT('Ctrl Pts',(-8.,-1.49674701985577E-14,-8.4));
#5096=CARTESIAN_POINT('Ctrl Pts',(-8.,2.14359353946684,-8.4));
#5097=CARTESIAN_POINT('Ctrl Pts',(-8.,4.61880215356146,-7.68546882017084));
#5098=CARTESIAN_POINT('Ctrl Pts',(-8.,-4.61880215356146,-7.68546882017084));
#5099=CARTESIAN_POINT('Ctrl Pts',(-8.,-2.14359353946686,-8.4));
#5100=CARTESIAN_POINT('Ctrl Pts',(-8.,-1.49674701985577E-14,-8.4));
#5101=CARTESIAN_POINT('Origin',(-1.73472347597681E-15,9.23760430703403,
0.));
#5102=CARTESIAN_POINT('Origin',(0.,0.,0.));
#5103=CARTESIAN_POINT('Origin',(0.,0.,0.));
#5104=CARTESIAN_POINT('Origin',(0.,0.,0.));
#5105=CARTESIAN_POINT('Origin',(0.,0.,0.));
#5106=CARTESIAN_POINT('Origin',(0.,0.,0.));
#5107=CARTESIAN_POINT('Origin',(0.,0.,0.));
#5108=CARTESIAN_POINT('Origin',(-1.73472347597681E-15,9.23760430703403,
-8.4));
#5109=CARTESIAN_POINT('Origin',(0.,0.,-8.4));
#5110=CARTESIAN_POINT('Origin',(0.,0.,-8.4));
#5111=CARTESIAN_POINT('Origin',(0.,0.,-8.4));
#5112=CARTESIAN_POINT('Origin',(0.,0.,-8.4));
#5113=CARTESIAN_POINT('Origin',(0.,0.,-8.4));
#5114=CARTESIAN_POINT('Origin',(0.,0.,-8.4));
#5115=CARTESIAN_POINT('Origin',(0.,0.,-8.4));
#5116=CARTESIAN_POINT('Origin',(0.,0.,-8.4));
#5117=CARTESIAN_POINT('Origin',(0.,0.,-8.4));
#5118=CARTESIAN_POINT('Origin',(0.,0.,-8.4));
#5119=CARTESIAN_POINT('Origin',(0.,0.,-8.4));
#5120=CARTESIAN_POINT('Origin',(0.,0.,-8.4));
#5121=CARTESIAN_POINT('Origin',(0.,0.,0.));
#5122=CARTESIAN_POINT('Origin',(0.,0.,0.));
#5123=CARTESIAN_POINT('Origin',(0.,0.,0.));
#5124=CARTESIAN_POINT('Origin',(0.,0.,0.));
#5125=CARTESIAN_POINT('Origin',(0.,0.,0.));
#5126=CARTESIAN_POINT('Origin',(0.,0.,0.));
#5638=UNCERTAINTY_MEASURE_WITH_UNIT(LENGTH_MEASURE(0.01),#5659,
'DISTANCE_ACCURACY_VALUE',
'Maximum model space distance between geometric entities at asserted c
onnectivities');
#5645=UNCERTAINTY_MEASURE_WITH_UNIT(LENGTH_MEASURE(0.01),#5659,
'DISTANCE_ACCURACY_VALUE',
'Maximum model space distance between geometric entities at asserted c
onnectivities');
#5651=(
GEOMETRIC_REPRESENTATION_CONTEXT(3)
GLOBAL_UNCERTAINTY_ASSIGNED_CONTEXT((#5638))
GLOBAL_UNIT_ASSIGNED_CONTEXT((#5659,#5661,#5662))
REPRESENTATION_CONTEXT('','3D')
);
#5658=(
GEOMETRIC_REPRESENTATION_CONTEXT(3)
GLOBAL_UNCERTAINTY_ASSIGNED_CONTEXT((#5645))
GLOBAL_UNIT_ASSIGNED_CONTEXT((#5659,#5661,#5662))
REPRESENTATION_CONTEXT('','3D')
);
#5659=(
LENGTH_UNIT()
NAMED_UNIT(*)
SI_UNIT(.MILLI.,.METRE.)
);
#5661=(
NAMED_UNIT(*)
PLANE_ANGLE_UNIT()
SI_UNIT($,.RADIAN.)
);
#5662=(
NAMED_UNIT(*)
SI_UNIT($,.STERADIAN.)
SOLID_ANGLE_UNIT()
);
#5668=SHAPE_DEFINITION_REPRESENTATION(#5680,#5710);
#5680=PRODUCT_DEFINITION_SHAPE('',$,#5723);
#5710=SHAPE_REPRESENTATION('',(#3325),#5651);
#5717=PRODUCT_DEFINITION_CONTEXT('part definition',#5755,'design');
#5723=PRODUCT_DEFINITION('Hex Nut M10 x 1.5 (2)',
'Hex Nut M10 x 1.5 (2)',#5735,#5717);
#5735=PRODUCT_DEFINITION_FORMATION('',$,#5762);
#5755=APPLICATION_CONTEXT(
'Core Data for Automotive Mechanical Design Process');
#5756=PRODUCT_CONTEXT('part definition',#5755,'mechanical');
#5762=PRODUCT('Hex Nut M10 x 1.5 (2)','Hex Nut M10 x 1.5 (2)',$,(#5756));
#5770=PRESENTATION_STYLE_ASSIGNMENT((#5775));
#5775=SURFACE_STYLE_USAGE(.BOTH.,#5780);
#5780=SURFACE_SIDE_STYLE('',(#5785));
#5785=SURFACE_STYLE_FILL_AREA(#5790);
#5790=FILL_AREA_STYLE('Opaque(31,36,43)',(#5795));
#5795=FILL_AREA_STYLE_COLOUR('Opaque(31,36,43)',#5800);
#5800=COLOUR_RGB('Opaque(31,36,43)',0.12156862745098,0.141176470588235,
0.168627450980392);
ENDSEC;
END-ISO-10303-21;
